ISO-10303-21;
HEADER;
/* Generated by software containing ST-Developer
 * from STEP Tools, Inc. (www.steptools.com) 
 */
/* OPTION: using custom renumber hook */

FILE_DESCRIPTION(
/* description */ ('STEP AP242 Edition 2', 'CAx-IF Rec.Pracs.---Representation and Presentation of Product Manufa
cturing Information (PMI)---4.0---2014-10-13', 'CAx-IF Rec.Pracs.---3D Tessellated Geometry---0.4---2014-09-14', '2;1', 'CAx-IF Rec.Pracs.---User Defined Attributes---1.5---2016-08-15'),
/* implementation_level */ '2;1');

FILE_NAME(
/* name */ 'bottle_premium_cover.step',
/* time_stamp */ '2026-10-08T12:15:07Z',
/* author */ (''),
/* organization */ (''),
/* preprocessor_version */ 'ST-DEVELOPER v20',
/* originating_system */ 'ONSHAPE BY PTC INC, 1.221',
/* authorisation */ '  ');

FILE_SCHEMA (('AP242_MANAGED_MODEL_BASED_3D_ENGINEERING_MIM_LF { 1 0 10303 442 3 1 4 }'));
ENDSEC;

DATA;
#60=COLOUR_RGB('', 0.66274510, 0.83137255, 0.94901961);
#222=SHAPE_REPRESENTATION_RELATIONSHIP('','',#13796,#249);
#249=ADVANCED_BREP_SHAPE_REPRESENTATION('',(#13740),#45486);
#926=CIRCLE('',#15002,0.001);
#927=CIRCLE('',#15003,0.001);
#928=CIRCLE('',#15007,0.001);
#929=CIRCLE('',#15009,0.001);
#930=CIRCLE('',#15010,0.001);
#931=CIRCLE('',#15014,0.001);
#932=CIRCLE('',#15016,0.001);
#933=CIRCLE('',#15017,0.001);
#934=CIRCLE('',#15021,0.001);
#935=CIRCLE('',#15023,0.00400000000000265);
#936=CIRCLE('',#15024,0.05);
#937=CIRCLE('',#15025,0.00400000000000387);
#938=CIRCLE('',#15026,0.004);
#939=CIRCLE('',#15027,0.00755);
#940=CIRCLE('',#15028,0.001);
#941=CIRCLE('',#15029,0.001);
#942=CIRCLE('',#15030,0.001);
#943=CIRCLE('',#15031,0.01);
#944=CIRCLE('',#15033,0.00400000000000265);
#945=CIRCLE('',#15034,0.05);
#946=CIRCLE('',#15035,0.00400000000000387);
#947=CIRCLE('',#15036,0.004);
#948=CIRCLE('',#15037,0.00755);
#949=CIRCLE('',#15038,0.01);
#1464=PLANE('',#15001);
#1465=PLANE('',#15004);
#1466=PLANE('',#15005);
#1467=PLANE('',#15008);
#1468=PLANE('',#15011);
#1469=PLANE('',#15012);
#1470=PLANE('',#15015);
#1471=PLANE('',#15018);
#1472=PLANE('',#15019);
#1473=PLANE('',#15022);
#1474=PLANE('',#15032);
#1767=CYLINDRICAL_SURFACE('',#15006,0.001);
#1768=CYLINDRICAL_SURFACE('',#15013,0.001);
#1769=CYLINDRICAL_SURFACE('',#15020,0.001);
#1770=CYLINDRICAL_SURFACE('',#15039,0.05);
#1771=CYLINDRICAL_SURFACE('',#15040,0.00400000000000387);
#1772=CYLINDRICAL_SURFACE('',#15041,0.004);
#1773=CYLINDRICAL_SURFACE('',#15042,0.00755);
#1774=CYLINDRICAL_SURFACE('',#15043,0.00400000000000265);
#1775=CYLINDRICAL_SURFACE('',#15044,0.001);
#1776=CYLINDRICAL_SURFACE('',#15045,0.001);
#1777=CYLINDRICAL_SURFACE('',#15046,0.001);
#1778=CYLINDRICAL_SURFACE('',#15047,0.01);
#4756=ORIENTED_EDGE('',*,*,#7025,.T.);
#4757=ORIENTED_EDGE('',*,*,#7026,.T.);
#4758=ORIENTED_EDGE('',*,*,#7027,.T.);
#4759=ORIENTED_EDGE('',*,*,#7028,.T.);
#4760=ORIENTED_EDGE('',*,*,#7029,.F.);
#4761=ORIENTED_EDGE('',*,*,#7030,.F.);
#4762=ORIENTED_EDGE('',*,*,#7028,.F.);
#4763=ORIENTED_EDGE('',*,*,#7031,.T.);
#4764=ORIENTED_EDGE('',*,*,#7032,.F.);
#4765=ORIENTED_EDGE('',*,*,#7033,.F.);
#4766=ORIENTED_EDGE('',*,*,#7026,.F.);
#4767=ORIENTED_EDGE('',*,*,#7034,.T.);
#4768=ORIENTED_EDGE('',*,*,#7035,.F.);
#4769=ORIENTED_EDGE('',*,*,#7034,.F.);
#4770=ORIENTED_EDGE('',*,*,#7025,.F.);
#4771=ORIENTED_EDGE('',*,*,#7030,.T.);
#4772=ORIENTED_EDGE('',*,*,#7036,.T.);
#4773=ORIENTED_EDGE('',*,*,#7037,.T.);
#4774=ORIENTED_EDGE('',*,*,#7038,.T.);
#4775=ORIENTED_EDGE('',*,*,#7039,.T.);
#4776=ORIENTED_EDGE('',*,*,#7040,.F.);
#4777=ORIENTED_EDGE('',*,*,#7041,.F.);
#4778=ORIENTED_EDGE('',*,*,#7039,.F.);
#4779=ORIENTED_EDGE('',*,*,#7042,.T.);
#4780=ORIENTED_EDGE('',*,*,#7043,.F.);
#4781=ORIENTED_EDGE('',*,*,#7044,.F.);
#4782=ORIENTED_EDGE('',*,*,#7037,.F.);
#4783=ORIENTED_EDGE('',*,*,#7045,.T.);
#4784=ORIENTED_EDGE('',*,*,#7046,.F.);
#4785=ORIENTED_EDGE('',*,*,#7045,.F.);
#4786=ORIENTED_EDGE('',*,*,#7036,.F.);
#4787=ORIENTED_EDGE('',*,*,#7041,.T.);
#4788=ORIENTED_EDGE('',*,*,#7047,.T.);
#4789=ORIENTED_EDGE('',*,*,#7048,.T.);
#4790=ORIENTED_EDGE('',*,*,#7049,.T.);
#4791=ORIENTED_EDGE('',*,*,#7050,.T.);
#4792=ORIENTED_EDGE('',*,*,#7051,.F.);
#4793=ORIENTED_EDGE('',*,*,#7052,.F.);
#4794=ORIENTED_EDGE('',*,*,#7050,.F.);
#4795=ORIENTED_EDGE('',*,*,#7053,.T.);
#4796=ORIENTED_EDGE('',*,*,#7054,.F.);
#4797=ORIENTED_EDGE('',*,*,#7055,.F.);
#4798=ORIENTED_EDGE('',*,*,#7048,.F.);
#4799=ORIENTED_EDGE('',*,*,#7056,.T.);
#4800=ORIENTED_EDGE('',*,*,#7057,.F.);
#4801=ORIENTED_EDGE('',*,*,#7056,.F.);
#4802=ORIENTED_EDGE('',*,*,#7047,.F.);
#4803=ORIENTED_EDGE('',*,*,#7052,.T.);
#4804=ORIENTED_EDGE('',*,*,#7058,.F.);
#4805=ORIENTED_EDGE('',*,*,#7059,.F.);
#4806=ORIENTED_EDGE('',*,*,#7060,.F.);
#4807=ORIENTED_EDGE('',*,*,#7061,.F.);
#4808=ORIENTED_EDGE('',*,*,#7062,.F.);
#4809=ORIENTED_EDGE('',*,*,#7054,.T.);
#4810=ORIENTED_EDGE('',*,*,#7057,.T.);
#4811=ORIENTED_EDGE('',*,*,#7051,.T.);
#4812=ORIENTED_EDGE('',*,*,#7063,.T.);
#4813=ORIENTED_EDGE('',*,*,#7043,.T.);
#4814=ORIENTED_EDGE('',*,*,#7046,.T.);
#4815=ORIENTED_EDGE('',*,*,#7040,.T.);
#4816=ORIENTED_EDGE('',*,*,#7064,.T.);
#4817=ORIENTED_EDGE('',*,*,#7032,.T.);
#4818=ORIENTED_EDGE('',*,*,#7035,.T.);
#4819=ORIENTED_EDGE('',*,*,#7029,.T.);
#4820=ORIENTED_EDGE('',*,*,#7065,.T.);
#4821=ORIENTED_EDGE('',*,*,#7066,.T.);
#4822=ORIENTED_EDGE('',*,*,#7067,.T.);
#4823=ORIENTED_EDGE('',*,*,#7068,.T.);
#4824=ORIENTED_EDGE('',*,*,#7069,.T.);
#4825=ORIENTED_EDGE('',*,*,#7070,.T.);
#4826=ORIENTED_EDGE('',*,*,#7071,.T.);
#4827=ORIENTED_EDGE('',*,*,#7072,.F.);
#4828=ORIENTED_EDGE('',*,*,#7059,.T.);
#4829=ORIENTED_EDGE('',*,*,#7068,.F.);
#4830=ORIENTED_EDGE('',*,*,#7060,.T.);
#4831=ORIENTED_EDGE('',*,*,#7069,.F.);
#4832=ORIENTED_EDGE('',*,*,#7061,.T.);
#4833=ORIENTED_EDGE('',*,*,#7070,.F.);
#4834=ORIENTED_EDGE('',*,*,#7062,.T.);
#4835=ORIENTED_EDGE('',*,*,#7071,.F.);
#4836=ORIENTED_EDGE('',*,*,#7058,.T.);
#4837=ORIENTED_EDGE('',*,*,#7067,.F.);
#4838=ORIENTED_EDGE('',*,*,#7049,.F.);
#4839=ORIENTED_EDGE('',*,*,#7055,.T.);
#4840=ORIENTED_EDGE('',*,*,#7063,.F.);
#4841=ORIENTED_EDGE('',*,*,#7053,.F.);
#4842=ORIENTED_EDGE('',*,*,#7038,.F.);
#4843=ORIENTED_EDGE('',*,*,#7044,.T.);
#4844=ORIENTED_EDGE('',*,*,#7064,.F.);
#4845=ORIENTED_EDGE('',*,*,#7042,.F.);
#4846=ORIENTED_EDGE('',*,*,#7027,.F.);
#4847=ORIENTED_EDGE('',*,*,#7033,.T.);
#4848=ORIENTED_EDGE('',*,*,#7065,.F.);
#4849=ORIENTED_EDGE('',*,*,#7031,.F.);
#4850=ORIENTED_EDGE('',*,*,#7072,.T.);
#4851=ORIENTED_EDGE('',*,*,#7066,.F.);
#7025=EDGE_CURVE('',#8468,#8469,#926,.T.);
#7026=EDGE_CURVE('',#8469,#8470,#9391,.T.);
#7027=EDGE_CURVE('',#8470,#8471,#927,.T.);
#7028=EDGE_CURVE('',#8471,#8468,#9392,.T.);
#7029=EDGE_CURVE('',#8472,#8473,#9393,.T.);
#7030=EDGE_CURVE('',#8468,#8472,#9394,.T.);
#7031=EDGE_CURVE('',#8471,#8473,#9395,.T.);
#7032=EDGE_CURVE('',#8474,#8475,#9396,.T.);
#7033=EDGE_CURVE('',#8470,#8474,#9397,.T.);
#7034=EDGE_CURVE('',#8469,#8475,#9398,.T.);
#7035=EDGE_CURVE('',#8475,#8472,#928,.T.);
#7036=EDGE_CURVE('',#8476,#8477,#929,.T.);
#7037=EDGE_CURVE('',#8477,#8478,#9399,.T.);
#7038=EDGE_CURVE('',#8478,#8479,#930,.T.);
#7039=EDGE_CURVE('',#8479,#8476,#9400,.T.);
#7040=EDGE_CURVE('',#8480,#8481,#9401,.T.);
#7041=EDGE_CURVE('',#8476,#8480,#9402,.T.);
#7042=EDGE_CURVE('',#8479,#8481,#9403,.T.);
#7043=EDGE_CURVE('',#8482,#8483,#9404,.T.);
#7044=EDGE_CURVE('',#8478,#8482,#9405,.T.);
#7045=EDGE_CURVE('',#8477,#8483,#9406,.T.);
#7046=EDGE_CURVE('',#8483,#8480,#931,.T.);
#7047=EDGE_CURVE('',#8484,#8485,#932,.T.);
#7048=EDGE_CURVE('',#8485,#8486,#9407,.T.);
#7049=EDGE_CURVE('',#8486,#8487,#933,.T.);
#7050=EDGE_CURVE('',#8487,#8484,#9408,.T.);
#7051=EDGE_CURVE('',#8488,#8489,#9409,.T.);
#7052=EDGE_CURVE('',#8484,#8488,#9410,.T.);
#7053=EDGE_CURVE('',#8487,#8489,#9411,.T.);
#7054=EDGE_CURVE('',#8490,#8491,#9412,.T.);
#7055=EDGE_CURVE('',#8486,#8490,#9413,.T.);
#7056=EDGE_CURVE('',#8485,#8491,#9414,.T.);
#7057=EDGE_CURVE('',#8491,#8488,#934,.T.);
#7058=EDGE_CURVE('',#8492,#8492,#935,.T.);
#7059=EDGE_CURVE('',#8493,#8493,#936,.T.);
#7060=EDGE_CURVE('',#8494,#8494,#937,.T.);
#7061=EDGE_CURVE('',#8495,#8495,#938,.T.);
#7062=EDGE_CURVE('',#8496,#8496,#939,.T.);
#7063=EDGE_CURVE('',#8489,#8490,#940,.T.);
#7064=EDGE_CURVE('',#8481,#8482,#941,.T.);
#7065=EDGE_CURVE('',#8473,#8474,#942,.T.);
#7066=EDGE_CURVE('',#8497,#8497,#943,.T.);
#7067=EDGE_CURVE('',#8498,#8498,#944,.T.);
#7068=EDGE_CURVE('',#8499,#8499,#945,.T.);
#7069=EDGE_CURVE('',#8500,#8500,#946,.T.);
#7070=EDGE_CURVE('',#8501,#8501,#947,.T.);
#7071=EDGE_CURVE('',#8502,#8502,#948,.T.);
#7072=EDGE_CURVE('',#8503,#8503,#949,.T.);
#8468=VERTEX_POINT('',#39465);
#8469=VERTEX_POINT('',#39466);
#8470=VERTEX_POINT('',#39468);
#8471=VERTEX_POINT('',#39470);
#8472=VERTEX_POINT('',#39474);
#8473=VERTEX_POINT('',#39475);
#8474=VERTEX_POINT('',#39480);
#8475=VERTEX_POINT('',#39481);
#8476=VERTEX_POINT('',#39488);
#8477=VERTEX_POINT('',#39489);
#8478=VERTEX_POINT('',#39491);
#8479=VERTEX_POINT('',#39493);
#8480=VERTEX_POINT('',#39497);
#8481=VERTEX_POINT('',#39498);
#8482=VERTEX_POINT('',#39503);
#8483=VERTEX_POINT('',#39504);
#8484=VERTEX_POINT('',#39511);
#8485=VERTEX_POINT('',#39512);
#8486=VERTEX_POINT('',#39514);
#8487=VERTEX_POINT('',#39516);
#8488=VERTEX_POINT('',#39520);
#8489=VERTEX_POINT('',#39521);
#8490=VERTEX_POINT('',#39526);
#8491=VERTEX_POINT('',#39527);
#8492=VERTEX_POINT('',#39534);
#8493=VERTEX_POINT('',#39536);
#8494=VERTEX_POINT('',#39538);
#8495=VERTEX_POINT('',#39540);
#8496=VERTEX_POINT('',#39542);
#8497=VERTEX_POINT('',#39547);
#8498=VERTEX_POINT('',#39550);
#8499=VERTEX_POINT('',#39552);
#8500=VERTEX_POINT('',#39554);
#8501=VERTEX_POINT('',#39556);
#8502=VERTEX_POINT('',#39558);
#8503=VERTEX_POINT('',#39560);
#9391=LINE('',#39467,#10219);
#9392=LINE('',#39471,#10220);
#9393=LINE('',#39473,#10221);
#9394=LINE('',#39476,#10222);
#9395=LINE('',#39477,#10223);
#9396=LINE('',#39479,#10224);
#9397=LINE('',#39482,#10225);
#9398=LINE('',#39483,#10226);
#9399=LINE('',#39490,#10227);
#9400=LINE('',#39494,#10228);
#9401=LINE('',#39496,#10229);
#9402=LINE('',#39499,#10230);
#9403=LINE('',#39500,#10231);
#9404=LINE('',#39502,#10232);
#9405=LINE('',#39505,#10233);
#9406=LINE('',#39506,#10234);
#9407=LINE('',#39513,#10235);
#9408=LINE('',#39517,#10236);
#9409=LINE('',#39519,#10237);
#9410=LINE('',#39522,#10238);
#9411=LINE('',#39523,#10239);
#9412=LINE('',#39525,#10240);
#9413=LINE('',#39528,#10241);
#9414=LINE('',#39529,#10242);
#10219=VECTOR('',#18315,1.);
#10220=VECTOR('',#18318,1.);
#10221=VECTOR('',#18321,1.);
#10222=VECTOR('',#18322,1.);
#10223=VECTOR('',#18323,1.);
#10224=VECTOR('',#18326,1.);
#10225=VECTOR('',#18327,1.);
#10226=VECTOR('',#18328,1.);
#10227=VECTOR('',#18337,1.);
#10228=VECTOR('',#18340,1.);
#10229=VECTOR('',#18343,1.);
#10230=VECTOR('',#18344,1.);
#10231=VECTOR('',#18345,1.);
#10232=VECTOR('',#18348,1.);
#10233=VECTOR('',#18349,1.);
#10234=VECTOR('',#18350,1.);
#10235=VECTOR('',#18359,1.);
#10236=VECTOR('',#18362,1.);
#10237=VECTOR('',#18365,1.);
#10238=VECTOR('',#18366,1.);
#10239=VECTOR('',#18367,1.);
#10240=VECTOR('',#18370,1.);
#10241=VECTOR('',#18371,1.);
#10242=VECTOR('',#18372,1.);
#11320=EDGE_LOOP('',(#4756,#4757,#4758,#4759));
#11321=EDGE_LOOP('',(#4760,#4761,#4762,#4763));
#11322=EDGE_LOOP('',(#4764,#4765,#4766,#4767));
#11323=EDGE_LOOP('',(#4768,#4769,#4770,#4771));
#11324=EDGE_LOOP('',(#4772,#4773,#4774,#4775));
#11325=EDGE_LOOP('',(#4776,#4777,#4778,#4779));
#11326=EDGE_LOOP('',(#4780,#4781,#4782,#4783));
#11327=EDGE_LOOP('',(#4784,#4785,#4786,#4787));
#11328=EDGE_LOOP('',(#4788,#4789,#4790,#4791));
#11329=EDGE_LOOP('',(#4792,#4793,#4794,#4795));
#11330=EDGE_LOOP('',(#4796,#4797,#4798,#4799));
#11331=EDGE_LOOP('',(#4800,#4801,#4802,#4803));
#11332=EDGE_LOOP('',(#4804));
#11333=EDGE_LOOP('',(#4805));
#11334=EDGE_LOOP('',(#4806));
#11335=EDGE_LOOP('',(#4807));
#11336=EDGE_LOOP('',(#4808));
#11337=EDGE_LOOP('',(#4809,#4810,#4811,#4812));
#11338=EDGE_LOOP('',(#4813,#4814,#4815,#4816));
#11339=EDGE_LOOP('',(#4817,#4818,#4819,#4820));
#11340=EDGE_LOOP('',(#4821));
#11341=EDGE_LOOP('',(#4822));
#11342=EDGE_LOOP('',(#4823));
#11343=EDGE_LOOP('',(#4824));
#11344=EDGE_LOOP('',(#4825));
#11345=EDGE_LOOP('',(#4826));
#11346=EDGE_LOOP('',(#4827));
#11347=EDGE_LOOP('',(#4828));
#11348=EDGE_LOOP('',(#4829));
#11349=EDGE_LOOP('',(#4830));
#11350=EDGE_LOOP('',(#4831));
#11351=EDGE_LOOP('',(#4832));
#11352=EDGE_LOOP('',(#4833));
#11353=EDGE_LOOP('',(#4834));
#11354=EDGE_LOOP('',(#4835));
#11355=EDGE_LOOP('',(#4836));
#11356=EDGE_LOOP('',(#4837));
#11357=EDGE_LOOP('',(#4838,#4839,#4840,#4841));
#11358=EDGE_LOOP('',(#4842,#4843,#4844,#4845));
#11359=EDGE_LOOP('',(#4846,#4847,#4848,#4849));
#11360=EDGE_LOOP('',(#4850));
#11361=EDGE_LOOP('',(#4851));
#12439=FACE_BOUND('',#11320,.T.);
#12440=FACE_BOUND('',#11321,.T.);
#12441=FACE_BOUND('',#11322,.T.);
#12442=FACE_BOUND('',#11323,.T.);
#12443=FACE_BOUND('',#11324,.T.);
#12444=FACE_BOUND('',#11325,.T.);
#12445=FACE_BOUND('',#11326,.T.);
#12446=FACE_BOUND('',#11327,.T.);
#12447=FACE_BOUND('',#11328,.T.);
#12448=FACE_BOUND('',#11329,.T.);
#12449=FACE_BOUND('',#11330,.T.);
#12450=FACE_BOUND('',#11331,.T.);
#12451=FACE_BOUND('',#11332,.T.);
#12452=FACE_BOUND('',#11333,.T.);
#12453=FACE_BOUND('',#11334,.T.);
#12454=FACE_BOUND('',#11335,.T.);
#12455=FACE_BOUND('',#11336,.T.);
#12456=FACE_BOUND('',#11337,.T.);
#12457=FACE_BOUND('',#11338,.T.);
#12458=FACE_BOUND('',#11339,.T.);
#12459=FACE_BOUND('',#11340,.T.);
#12460=FACE_BOUND('',#11341,.T.);
#12461=FACE_BOUND('',#11342,.T.);
#12462=FACE_BOUND('',#11343,.T.);
#12463=FACE_BOUND('',#11344,.T.);
#12464=FACE_BOUND('',#11345,.T.);
#12465=FACE_BOUND('',#11346,.T.);
#12466=FACE_BOUND('',#11347,.T.);
#12467=FACE_BOUND('',#11348,.T.);
#12468=FACE_BOUND('',#11349,.T.);
#12469=FACE_BOUND('',#11350,.T.);
#12470=FACE_BOUND('',#11351,.T.);
#12471=FACE_BOUND('',#11352,.T.);
#12472=FACE_BOUND('',#11353,.T.);
#12473=FACE_BOUND('',#11354,.T.);
#12474=FACE_BOUND('',#11355,.T.);
#12475=FACE_BOUND('',#11356,.T.);
#12476=FACE_BOUND('',#11357,.T.);
#12477=FACE_BOUND('',#11358,.T.);
#12478=FACE_BOUND('',#11359,.T.);
#12479=FACE_BOUND('',#11360,.T.);
#12480=FACE_BOUND('',#11361,.T.);
#13333=ADVANCED_FACE('',(#12439),#1464,.F.);
#13334=ADVANCED_FACE('',(#12440),#1465,.T.);
#13335=ADVANCED_FACE('',(#12441),#1466,.T.);
#13336=ADVANCED_FACE('',(#12442),#1767,.T.);
#13337=ADVANCED_FACE('',(#12443),#1467,.F.);
#13338=ADVANCED_FACE('',(#12444),#1468,.T.);
#13339=ADVANCED_FACE('',(#12445),#1469,.T.);
#13340=ADVANCED_FACE('',(#12446),#1768,.T.);
#13341=ADVANCED_FACE('',(#12447),#1470,.F.);
#13342=ADVANCED_FACE('',(#12448),#1471,.T.);
#13343=ADVANCED_FACE('',(#12449),#1472,.T.);
#13344=ADVANCED_FACE('',(#12450),#1769,.T.);
#13345=ADVANCED_FACE('',(#12451,#12452,#12453,#12454,#12455,#12456,#12457,
#12458,#12459),#1473,.F.);
#13346=ADVANCED_FACE('',(#12460,#12461,#12462,#12463,#12464,#12465),#1474,
 .T.);
#13347=ADVANCED_FACE('',(#12466,#12467),#1770,.T.);
#13348=ADVANCED_FACE('',(#12468,#12469),#1771,.F.);
#13349=ADVANCED_FACE('',(#12470,#12471),#1772,.F.);
#13350=ADVANCED_FACE('',(#12472,#12473),#1773,.F.);
#13351=ADVANCED_FACE('',(#12474,#12475),#1774,.F.);
#13352=ADVANCED_FACE('',(#12476),#1775,.T.);
#13353=ADVANCED_FACE('',(#12477),#1776,.T.);
#13354=ADVANCED_FACE('',(#12478),#1777,.T.);
#13355=ADVANCED_FACE('',(#12479,#12480),#1778,.F.);
#13523=CLOSED_SHELL('',(#13333,#13334,#13335,#13336,#13337,#13338,#13339,
#13340,#13341,#13342,#13343,#13344,#13345,#13346,#13347,#13348,#13349,#13350,
#13351,#13352,#13353,#13354,#13355));
#13550=STYLED_ITEM('',(#13577),#13740);
#13577=PRESENTATION_STYLE_ASSIGNMENT((#13604));
#13604=SURFACE_STYLE_USAGE(.BOTH.,#13631);
#13631=SURFACE_SIDE_STYLE('',(#13658));
#13658=SURFACE_STYLE_FILL_AREA(#13685);
#13685=FILL_AREA_STYLE('',(#13712));
#13712=FILL_AREA_STYLE_COLOUR('',#60);
#13740=MANIFOLD_SOLID_BREP('bottle_premium_cover',#13523);
#13768=SHAPE_DEFINITION_REPRESENTATION(#45572,#13796);
#13796=SHAPE_REPRESENTATION('bottle_premium_cover',(#13802),#45486);
#13802=AXIS2_PLACEMENT_3D('',#19109,#15295,#15296);
#15001=AXIS2_PLACEMENT_3D('',#39463,#18311,#18312);
#15002=AXIS2_PLACEMENT_3D('',#39464,#18313,#18314);
#15003=AXIS2_PLACEMENT_3D('',#39469,#18316,#18317);
#15004=AXIS2_PLACEMENT_3D('',#39472,#18319,#18320);
#15005=AXIS2_PLACEMENT_3D('',#39478,#18324,#18325);
#15006=AXIS2_PLACEMENT_3D('',#39484,#18329,#18330);
#15007=AXIS2_PLACEMENT_3D('',#39485,#18331,#18332);
#15008=AXIS2_PLACEMENT_3D('',#39486,#18333,#18334);
#15009=AXIS2_PLACEMENT_3D('',#39487,#18335,#18336);
#15010=AXIS2_PLACEMENT_3D('',#39492,#18338,#18339);
#15011=AXIS2_PLACEMENT_3D('',#39495,#18341,#18342);
#15012=AXIS2_PLACEMENT_3D('',#39501,#18346,#18347);
#15013=AXIS2_PLACEMENT_3D('',#39507,#18351,#18352);
#15014=AXIS2_PLACEMENT_3D('',#39508,#18353,#18354);
#15015=AXIS2_PLACEMENT_3D('',#39509,#18355,#18356);
#15016=AXIS2_PLACEMENT_3D('',#39510,#18357,#18358);
#15017=AXIS2_PLACEMENT_3D('',#39515,#18360,#18361);
#15018=AXIS2_PLACEMENT_3D('',#39518,#18363,#18364);
#15019=AXIS2_PLACEMENT_3D('',#39524,#18368,#18369);
#15020=AXIS2_PLACEMENT_3D('',#39530,#18373,#18374);
#15021=AXIS2_PLACEMENT_3D('',#39531,#18375,#18376);
#15022=AXIS2_PLACEMENT_3D('',#39532,#18377,#18378);
#15023=AXIS2_PLACEMENT_3D('',#39533,#18379,#18380);
#15024=AXIS2_PLACEMENT_3D('',#39535,#18381,#18382);
#15025=AXIS2_PLACEMENT_3D('',#39537,#18383,#18384);
#15026=AXIS2_PLACEMENT_3D('',#39539,#18385,#18386);
#15027=AXIS2_PLACEMENT_3D('',#39541,#18387,#18388);
#15028=AXIS2_PLACEMENT_3D('',#39543,#18389,#18390);
#15029=AXIS2_PLACEMENT_3D('',#39544,#18391,#18392);
#15030=AXIS2_PLACEMENT_3D('',#39545,#18393,#18394);
#15031=AXIS2_PLACEMENT_3D('',#39546,#18395,#18396);
#15032=AXIS2_PLACEMENT_3D('',#39548,#18397,#18398);
#15033=AXIS2_PLACEMENT_3D('',#39549,#18399,#18400);
#15034=AXIS2_PLACEMENT_3D('',#39551,#18401,#18402);
#15035=AXIS2_PLACEMENT_3D('',#39553,#18403,#18404);
#15036=AXIS2_PLACEMENT_3D('',#39555,#18405,#18406);
#15037=AXIS2_PLACEMENT_3D('',#39557,#18407,#18408);
#15038=AXIS2_PLACEMENT_3D('',#39559,#18409,#18410);
#15039=AXIS2_PLACEMENT_3D('',#39561,#18411,#18412);
#15040=AXIS2_PLACEMENT_3D('',#39562,#18413,#18414);
#15041=AXIS2_PLACEMENT_3D('',#39563,#18415,#18416);
#15042=AXIS2_PLACEMENT_3D('',#39564,#18417,#18418);
#15043=AXIS2_PLACEMENT_3D('',#39565,#18419,#18420);
#15044=AXIS2_PLACEMENT_3D('',#39566,#18421,#18422);
#15045=AXIS2_PLACEMENT_3D('',#39567,#18423,#18424);
#15046=AXIS2_PLACEMENT_3D('',#39568,#18425,#18426);
#15047=AXIS2_PLACEMENT_3D('',#39569,#18427,#18428);
#15295=DIRECTION('',(0.,0.,1.));
#15296=DIRECTION('',(1.,0.,0.));
#18311=DIRECTION('',(0.,0.,1.));
#18312=DIRECTION('',(-0.5,0.866025403784436,0.));
#18313=DIRECTION('',(0.,0.,-1.));
#18314=DIRECTION('',(-0.499999999999993,-0.866025403784443,0.));
#18315=DIRECTION('',(-1.,-7.105427357601E-15,0.));
#18316=DIRECTION('',(0.,0.,-1.));
#18317=DIRECTION('',(-0.499999999999993,-0.866025403784443,0.));
#18318=DIRECTION('',(1.,6.55031584528842E-15,0.));
#18319=DIRECTION('',(0.,1.,0.));
#18320=DIRECTION('',(-1.,0.,0.));
#18321=DIRECTION('',(-1.,-6.55031584528842E-15,0.));
#18322=DIRECTION('',(0.,0.,1.));
#18323=DIRECTION('',(0.,0.,1.));
#18324=DIRECTION('',(0.,-1.,0.));
#18325=DIRECTION('',(1.,0.,0.));
#18326=DIRECTION('',(1.,7.105427357601E-15,0.));
#18327=DIRECTION('',(0.,0.,1.));
#18328=DIRECTION('',(0.,0.,1.));
#18329=DIRECTION('',(0.,0.,1.));
#18330=DIRECTION('',(-0.499999999999993,-0.866025403784443,0.));
#18331=DIRECTION('',(0.,0.,1.));
#18332=DIRECTION('',(-0.499999999999993,-0.866025403784443,0.));
#18333=DIRECTION('',(0.,0.,1.));
#18334=DIRECTION('',(-0.5,0.866025403784436,0.));
#18335=DIRECTION('',(0.,0.,-1.));
#18336=DIRECTION('',(-0.5,0.866025403784439,0.));
#18337=DIRECTION('',(0.5,0.86602540378444,0.));
#18338=DIRECTION('',(0.,0.,-1.));
#18339=DIRECTION('',(-0.5,0.866025403784436,0.));
#18340=DIRECTION('',(-0.5,-0.86602540378444,0.));
#18341=DIRECTION('',(0.86602540378444,-0.5,0.));
#18342=DIRECTION('',(0.5,0.86602540378444,0.));
#18343=DIRECTION('',(0.5,0.86602540378444,0.));
#18344=DIRECTION('',(0.,0.,1.));
#18345=DIRECTION('',(0.,0.,1.));
#18346=DIRECTION('',(-0.86602540378444,0.5,0.));
#18347=DIRECTION('',(-0.5,-0.86602540378444,0.));
#18348=DIRECTION('',(-0.5,-0.86602540378444,0.));
#18349=DIRECTION('',(0.,0.,1.));
#18350=DIRECTION('',(0.,0.,1.));
#18351=DIRECTION('',(0.,0.,1.));
#18352=DIRECTION('',(-0.5,0.866025403784436,0.));
#18353=DIRECTION('',(0.,0.,1.));
#18354=DIRECTION('',(-0.5,0.866025403784436,0.));
#18355=DIRECTION('',(0.,0.,1.));
#18356=DIRECTION('',(-0.5,0.866025403784436,0.));
#18357=DIRECTION('',(0.,0.,-1.));
#18358=DIRECTION('',(1.,0.,0.));
#18359=DIRECTION('',(0.5,-0.86602540378444,0.));
#18360=DIRECTION('',(0.,0.,-1.));
#18361=DIRECTION('',(1.,0.,0.));
#18362=DIRECTION('',(-0.5,0.86602540378444,0.));
#18363=DIRECTION('',(-0.86602540378444,-0.5,0.));
#18364=DIRECTION('',(0.5,-0.86602540378444,0.));
#18365=DIRECTION('',(0.5,-0.86602540378444,0.));
#18366=DIRECTION('',(0.,0.,1.));
#18367=DIRECTION('',(0.,0.,1.));
#18368=DIRECTION('',(0.86602540378444,0.5,0.));
#18369=DIRECTION('',(-0.5,0.86602540378444,0.));
#18370=DIRECTION('',(-0.5,0.86602540378444,0.));
#18371=DIRECTION('',(0.,0.,1.));
#18372=DIRECTION('',(0.,0.,1.));
#18373=DIRECTION('',(0.,0.,1.));
#18374=DIRECTION('',(1.,0.,0.));
#18375=DIRECTION('',(0.,0.,1.));
#18376=DIRECTION('',(1.,0.,0.));
#18377=DIRECTION('',(0.,0.,1.));
#18378=DIRECTION('',(1.,0.,0.));
#18379=DIRECTION('',(0.,0.,-1.));
#18380=DIRECTION('',(1.,0.,0.));
#18381=DIRECTION('',(0.,0.,1.));
#18382=DIRECTION('',(1.,0.,0.));
#18383=DIRECTION('',(0.,0.,-1.));
#18384=DIRECTION('',(1.,0.,0.));
#18385=DIRECTION('',(0.,0.,-1.));
#18386=DIRECTION('',(1.,0.,0.));
#18387=DIRECTION('',(0.,0.,-1.));
#18388=DIRECTION('',(1.,0.,0.));
#18389=DIRECTION('',(0.,0.,1.));
#18390=DIRECTION('',(1.,0.,0.));
#18391=DIRECTION('',(0.,0.,1.));
#18392=DIRECTION('',(-0.5,0.866025403784436,0.));
#18393=DIRECTION('',(0.,0.,1.));
#18394=DIRECTION('',(-0.499999999999993,-0.866025403784443,0.));
#18395=DIRECTION('',(0.,0.,1.));
#18396=DIRECTION('',(1.,0.,0.));
#18397=DIRECTION('',(0.,0.,1.));
#18398=DIRECTION('',(1.,0.,0.));
#18399=DIRECTION('',(0.,0.,-1.));
#18400=DIRECTION('',(1.,0.,0.));
#18401=DIRECTION('',(0.,0.,1.));
#18402=DIRECTION('',(1.,0.,0.));
#18403=DIRECTION('',(0.,0.,-1.));
#18404=DIRECTION('',(1.,0.,0.));
#18405=DIRECTION('',(0.,0.,-1.));
#18406=DIRECTION('',(1.,0.,0.));
#18407=DIRECTION('',(0.,0.,-1.));
#18408=DIRECTION('',(1.,0.,0.));
#18409=DIRECTION('',(0.,0.,1.));
#18410=DIRECTION('',(1.,0.,0.));
#18411=DIRECTION('',(0.,0.,-1.));
#18412=DIRECTION('',(-1.,0.,0.));
#18413=DIRECTION('',(0.,0.,-1.));
#18414=DIRECTION('',(-1.,0.,0.));
#18415=DIRECTION('',(0.,0.,-1.));
#18416=DIRECTION('',(-1.,0.,0.));
#18417=DIRECTION('',(0.,0.,-1.));
#18418=DIRECTION('',(-1.,0.,0.));
#18419=DIRECTION('',(0.,0.,-1.));
#18420=DIRECTION('',(-1.,0.,0.));
#18421=DIRECTION('',(0.,0.,1.));
#18422=DIRECTION('',(1.,0.,0.));
#18423=DIRECTION('',(0.,0.,1.));
#18424=DIRECTION('',(-0.5,0.866025403784436,0.));
#18425=DIRECTION('',(0.,0.,1.));
#18426=DIRECTION('',(-0.499999999999993,-0.866025403784443,0.));
#18427=DIRECTION('',(0.,0.,1.));
#18428=DIRECTION('',(1.,0.,0.));
#19109=CARTESIAN_POINT('',(0.,0.,0.));
#39463=CARTESIAN_POINT('',(0.,0.,0.081));
#39464=CARTESIAN_POINT('',(0.00350000000000027,-0.038,0.081));
#39465=CARTESIAN_POINT('',(0.00350000000000026,-0.037,0.081));
#39466=CARTESIAN_POINT('',(0.00350000000000028,-0.039,0.081));
#39467=CARTESIAN_POINT('',(0.00350000000000027,-0.039,0.081));
#39468=CARTESIAN_POINT('',(-0.00349999999999973,-0.039,0.081));
#39469=CARTESIAN_POINT('',(-0.00349999999999973,-0.038,0.081));
#39470=CARTESIAN_POINT('',(-0.00349999999999974,-0.037,0.081));
#39471=CARTESIAN_POINT('',(0.00350000000000026,-0.037,0.081));
#39472=CARTESIAN_POINT('',(0.00350000000000026,-0.037,0.0712404553740472));
#39473=CARTESIAN_POINT('',(2.393918396848E-16,-0.037,0.083));
#39474=CARTESIAN_POINT('',(0.00350000000000026,-0.037,0.083));
#39475=CARTESIAN_POINT('',(-0.00349999999999974,-0.037,0.083));
#39476=CARTESIAN_POINT('',(0.00350000000000026,-0.037,0.0712404553740472));
#39477=CARTESIAN_POINT('',(-0.00349999999999974,-0.037,0.0712404553740472));
#39478=CARTESIAN_POINT('',(0.00350000000000027,-0.039,0.0712404553740472));
#39479=CARTESIAN_POINT('',(2.74086309204335E-16,-0.039,0.083));
#39480=CARTESIAN_POINT('',(-0.00349999999999973,-0.039,0.083));
#39481=CARTESIAN_POINT('',(0.00350000000000028,-0.039,0.083));
#39482=CARTESIAN_POINT('',(-0.00349999999999972,-0.039,0.0712404553740472));
#39483=CARTESIAN_POINT('',(0.00350000000000027,-0.039,0.0712404553740472));
#39484=CARTESIAN_POINT('',(0.00350000000000027,-0.038,0.0712404553740472));
#39485=CARTESIAN_POINT('',(0.00350000000000027,-0.038,0.083));
#39486=CARTESIAN_POINT('',(0.,0.,0.081));
#39487=CARTESIAN_POINT('',(-0.0346589653438087,0.0159689110867544,0.081));
#39488=CARTESIAN_POINT('',(-0.0337929399400243,0.0154689110867544,0.081));
#39489=CARTESIAN_POINT('',(-0.0355249907475932,0.0164689110867544,0.081));
#39490=CARTESIAN_POINT('',(-0.0355249907475932,0.0164689110867544,0.081));
#39491=CARTESIAN_POINT('',(-0.0320249907475932,0.0225310889132454,0.081));
#39492=CARTESIAN_POINT('',(-0.0311589653438087,0.0220310889132454,0.081));
#39493=CARTESIAN_POINT('',(-0.0302929399400243,0.0215310889132454,0.081));
#39494=CARTESIAN_POINT('',(-0.0337929399400243,0.0154689110867544,0.081));
#39495=CARTESIAN_POINT('',(-0.0337929399400243,0.0154689110867544,0.0712404553740472));
#39496=CARTESIAN_POINT('',(-0.0320429399400243,0.0185,0.083));
#39497=CARTESIAN_POINT('',(-0.0337929399400243,0.0154689110867544,0.083));
#39498=CARTESIAN_POINT('',(-0.0302929399400243,0.0215310889132454,0.083));
#39499=CARTESIAN_POINT('',(-0.0337929399400243,0.0154689110867544,0.0712404553740472));
#39500=CARTESIAN_POINT('',(-0.0302929399400243,0.0215310889132454,0.0712404553740472));
#39501=CARTESIAN_POINT('',(-0.0355249907475932,0.0164689110867544,0.0712404553740472));
#39502=CARTESIAN_POINT('',(-0.0337749907475932,0.0195,0.083));
#39503=CARTESIAN_POINT('',(-0.0320249907475932,0.0225310889132454,0.083));
#39504=CARTESIAN_POINT('',(-0.0355249907475932,0.0164689110867544,0.083));
#39505=CARTESIAN_POINT('',(-0.0320249907475932,0.0225310889132454,0.0712404553740472));
#39506=CARTESIAN_POINT('',(-0.0355249907475932,0.0164689110867544,0.0712404553740472));
#39507=CARTESIAN_POINT('',(-0.0346589653438087,0.0159689110867544,0.0712404553740472));
#39508=CARTESIAN_POINT('',(-0.0346589653438087,0.0159689110867544,0.083));
#39509=CARTESIAN_POINT('',(0.,0.,0.081));
#39510=CARTESIAN_POINT('',(0.0311589653438087,0.0220310889132454,0.081));
#39511=CARTESIAN_POINT('',(0.0302929399400243,0.0215310889132454,0.081));
#39512=CARTESIAN_POINT('',(0.0320249907475932,0.0225310889132454,0.081));
#39513=CARTESIAN_POINT('',(0.0320249907475932,0.0225310889132454,0.081));
#39514=CARTESIAN_POINT('',(0.0355249907475932,0.0164689110867544,0.081));
#39515=CARTESIAN_POINT('',(0.0346589653438087,0.0159689110867544,0.081));
#39516=CARTESIAN_POINT('',(0.0337929399400242,0.0154689110867544,0.081));
#39517=CARTESIAN_POINT('',(0.0302929399400243,0.0215310889132454,0.081));
#39518=CARTESIAN_POINT('',(0.0302929399400243,0.0215310889132454,0.0712404553740472));
#39519=CARTESIAN_POINT('',(0.0320429399400243,0.0185,0.083));
#39520=CARTESIAN_POINT('',(0.0302929399400243,0.0215310889132454,0.083));
#39521=CARTESIAN_POINT('',(0.0337929399400242,0.0154689110867544,0.083));
#39522=CARTESIAN_POINT('',(0.0302929399400243,0.0215310889132454,0.0712404553740472));
#39523=CARTESIAN_POINT('',(0.0337929399400242,0.0154689110867544,0.0712404553740472));
#39524=CARTESIAN_POINT('',(0.0320249907475932,0.0225310889132454,0.0712404553740472));
#39525=CARTESIAN_POINT('',(0.0337749907475932,0.0195,0.083));
#39526=CARTESIAN_POINT('',(0.0355249907475932,0.0164689110867544,0.083));
#39527=CARTESIAN_POINT('',(0.0320249907475932,0.0225310889132454,0.083));
#39528=CARTESIAN_POINT('',(0.0355249907475932,0.0164689110867544,0.0712404553740472));
#39529=CARTESIAN_POINT('',(0.0320249907475932,0.0225310889132454,0.0712404553740472));
#39530=CARTESIAN_POINT('',(0.0311589653438087,0.0220310889132454,0.0712404553740472));
#39531=CARTESIAN_POINT('',(0.0311589653438087,0.0220310889132454,0.083));
#39532=CARTESIAN_POINT('',(0.,0.,0.083));
#39533=CARTESIAN_POINT('',(0.0259807621135363,-0.0149999999999982,0.083));
#39534=CARTESIAN_POINT('',(0.029980762113539,-0.0149999999999982,0.083));
#39535=CARTESIAN_POINT('',(0.,0.,0.083));
#39536=CARTESIAN_POINT('',(0.05,0.,0.083));
#39537=CARTESIAN_POINT('',(-0.02598076211353,-0.0150000000000018,0.083));
#39538=CARTESIAN_POINT('',(-0.0219807621135261,-0.0150000000000018,0.083));
#39539=CARTESIAN_POINT('',(0.,0.03,0.083));
#39540=CARTESIAN_POINT('',(0.004,0.03,0.083));
#39541=CARTESIAN_POINT('',(0.,0.,0.083));
#39542=CARTESIAN_POINT('',(0.00755,0.,0.083));
#39543=CARTESIAN_POINT('',(0.0346589653438087,0.0159689110867544,0.083));
#39544=CARTESIAN_POINT('',(-0.0311589653438087,0.0220310889132454,0.083));
#39545=CARTESIAN_POINT('',(-0.00349999999999973,-0.038,0.083));
#39546=CARTESIAN_POINT('',(-0.0175,0.0303108891324553,0.083));
#39547=CARTESIAN_POINT('',(-0.0075,0.0303108891324553,0.083));
#39548=CARTESIAN_POINT('',(0.,0.,0.084));
#39549=CARTESIAN_POINT('',(0.0259807621135363,-0.0149999999999982,0.084));
#39550=CARTESIAN_POINT('',(0.029980762113539,-0.0149999999999982,0.084));
#39551=CARTESIAN_POINT('',(0.,0.,0.084));
#39552=CARTESIAN_POINT('',(0.05,0.,0.084));
#39553=CARTESIAN_POINT('',(-0.02598076211353,-0.0150000000000018,0.084));
#39554=CARTESIAN_POINT('',(-0.0219807621135261,-0.0150000000000018,0.084));
#39555=CARTESIAN_POINT('',(0.,0.03,0.084));
#39556=CARTESIAN_POINT('',(0.004,0.03,0.084));
#39557=CARTESIAN_POINT('',(0.,0.,0.084));
#39558=CARTESIAN_POINT('',(0.00755,0.,0.084));
#39559=CARTESIAN_POINT('',(-0.0175,0.0303108891324553,0.084));
#39560=CARTESIAN_POINT('',(-0.0075,0.0303108891324553,0.084));
#39561=CARTESIAN_POINT('',(0.,0.,0.084));
#39562=CARTESIAN_POINT('',(-0.02598076211353,-0.0150000000000018,0.084));
#39563=CARTESIAN_POINT('',(0.,0.03,0.084));
#39564=CARTESIAN_POINT('',(0.,0.,0.084));
#39565=CARTESIAN_POINT('',(0.0259807621135363,-0.0149999999999982,0.084));
#39566=CARTESIAN_POINT('',(0.0346589653438087,0.0159689110867544,0.0712404553740472));
#39567=CARTESIAN_POINT('',(-0.0311589653438087,0.0220310889132454,0.0712404553740472));
#39568=CARTESIAN_POINT('',(-0.00349999999999973,-0.038,0.0712404553740472));
#39569=CARTESIAN_POINT('',(-0.0175,0.0303108891324553,0.074));
#45463=MECHANICAL_DESIGN_GEOMETRIC_PRESENTATION_REPRESENTATION('',(#13550),#45464);
#45464=(
GEOMETRIC_REPRESENTATION_CONTEXT(3)
GLOBAL_UNCERTAINTY_ASSIGNED_CONTEXT((#45492))
GLOBAL_UNIT_ASSIGNED_CONTEXT((#45522,#45521,#45520))
REPRESENTATION_CONTEXT('MAS-690','TOP_LEVEL_ASSEMBLY_PART')
);
#45486=(
GEOMETRIC_REPRESENTATION_CONTEXT(3)
GLOBAL_UNCERTAINTY_ASSIGNED_CONTEXT((#45514))
GLOBAL_UNIT_ASSIGNED_CONTEXT((#45522,#45521,#45520))
REPRESENTATION_CONTEXT('bottle_premium_cover','COMPONENT_PART')
);
#45492=UNCERTAINTY_MEASURE_WITH_UNIT(LENGTH_MEASURE(1.E-8),#45522,
'DISTANCE_ACCURACY_VALUE','Maximum Tolerance applied to model');
#45514=UNCERTAINTY_MEASURE_WITH_UNIT(LENGTH_MEASURE(1.E-6),#45522,
'DISTANCE_ACCURACY_VALUE','Maximum Tolerance applied to model');
#45520=(
NAMED_UNIT(*)
SI_UNIT($,.STERADIAN.)
SOLID_ANGLE_UNIT()
);
#45521=(
NAMED_UNIT(*)
PLANE_ANGLE_UNIT()
SI_UNIT($,.RADIAN.)
);
#45522=(
LENGTH_UNIT()
NAMED_UNIT(*)
SI_UNIT($,.METRE.)
);
#45572=PRODUCT_DEFINITION_SHAPE('','',#45607);
#45607=PRODUCT_DEFINITION('','',#45663,#45635);
#45635=PRODUCT_DEFINITION_CONTEXT('',#45782,'design');
#45663=PRODUCT_DEFINITION_FORMATION_WITH_SPECIFIED_SOURCE('','',#45719,
 .NOT_KNOWN.);
#45719=PRODUCT('bottle_premium_cover','bottle_premium_cover',
'bottle_premium_cover',(#45775));
#45775=PRODUCT_CONTEXT('',#45782,'mechanical');
#45782=APPLICATION_CONTEXT('managed model based 3d engineering');
ENDSEC;
END-ISO-10303-21;
